ISO-10303-21;
HEADER;
/* Generated by software containing ST-Developer
 * from STEP Tools, Inc. (www.steptools.com) 
 */

FILE_DESCRIPTION(
/* description */ ('STEP AP214'),
/* implementation_level */ '2;1');

FILE_NAME(
/* name */ 'Nut.step',
/* time_stamp */ '2026-11-14T21:46:24-08:00',
/* author */ (''),
/* organization */ (''),
/* preprocessor_version */ 'ST-DEVELOPER v20.2',
/* originating_system */ 'Autodesk Translation Framework v15.17.0.0',
/* authorisation */ '');

FILE_SCHEMA (('AUTOMOTIVE_DESIGN { 1 0 10303 214 3 1 1 }'));
ENDSEC;

DATA;
#10=MECHANICAL_DESIGN_GEOMETRIC_PRESENTATION_REPRESENTATION('',(#91),#7783);
#25=SPHERICAL_SURFACE('',#4400,7.25);
#26=SPHERICAL_SURFACE('',#4410,7.25);
#77=SHAPE_REPRESENTATION_RELATIONSHIP('SRR','None',#7822,#84);
#84=ADVANCED_BREP_SHAPE_REPRESENTATION('',(#98),#7778);
#91=STYLED_ITEM('',(#7869),#98);
#98=MANIFOLD_SOLID_BREP('Body1',#4166);
#123=FACE_BOUND('',#1436,.T.);
#124=FACE_BOUND('',#1438,.T.);
#125=FACE_BOUND('',#1440,.T.);
#126=FACE_BOUND('',#1442,.T.);
#127=FACE_BOUND('',#1444,.T.);
#128=FACE_BOUND('',#1446,.T.);
#129=FACE_BOUND('',#1448,.T.);
#130=FACE_BOUND('',#1450,.T.);
#131=FACE_BOUND('',#1452,.T.);
#132=FACE_BOUND('',#1454,.T.);
#133=FACE_BOUND('',#1457,.T.);
#134=FACE_BOUND('',#1462,.T.);
#135=FACE_BOUND('',#1472,.T.);
#136=FACE_BOUND('',#1474,.T.);
#218=PLANE('',#4423);
#219=PLANE('',#4424);
#220=PLANE('',#4425);
#221=PLANE('',#4427);
#222=PLANE('',#4429);
#223=PLANE('',#4431);
#224=PLANE('',#4433);
#225=PLANE('',#4435);
#226=PLANE('',#4437);
#227=PLANE('',#4439);
#228=PLANE('',#4441);
#229=PLANE('',#4442);
#230=PLANE('',#4443);
#231=PLANE('',#4444);
#232=PLANE('',#4445);
#233=PLANE('',#4446);
#234=PLANE('',#4447);
#235=PLANE('',#4448);
#236=PLANE('',#4453);
#237=PLANE('',#4454);
#238=PLANE('',#4455);
#239=PLANE('',#4456);
#240=PLANE('',#4457);
#241=PLANE('',#4458);
#242=PLANE('',#4459);
#243=PLANE('',#4460);
#439=LINE('',#6413,#798);
#440=LINE('',#6416,#799);
#441=LINE('',#6422,#800);
#442=LINE('',#6425,#801);
#443=LINE('',#6431,#802);
#444=LINE('',#6434,#803);
#445=LINE('',#6439,#804);
#446=LINE('',#6445,#805);
#447=LINE('',#6451,#806);
#448=LINE('',#6459,#807);
#449=LINE('',#6464,#808);
#450=LINE('',#6470,#809);
#451=LINE('',#6477,#810);
#452=LINE('',#6483,#811);
#453=LINE('',#6489,#812);
#454=LINE('',#6493,#813);
#455=LINE('',#6495,#814);
#456=LINE('',#6499,#815);
#457=LINE('',#6501,#816);
#458=LINE('',#6503,#817);
#459=LINE('',#6505,#818);
#460=LINE('',#6507,#819);
#461=LINE('',#6509,#820);
#462=LINE('',#6511,#821);
#463=LINE('',#6513,#822);
#464=LINE('',#6515,#823);
#465=LINE('',#6517,#824);
#466=LINE('',#6519,#825);
#467=LINE('',#6521,#826);
#468=LINE('',#6523,#827);
#469=LINE('',#6525,#828);
#470=LINE('',#6527,#829);
#471=LINE('',#6529,#830);
#472=LINE('',#6531,#831);
#473=LINE('',#6533,#832);
#474=LINE('',#6535,#833);
#475=LINE('',#6536,#834);
#476=LINE('',#6540,#835);
#477=LINE('',#6542,#836);
#478=LINE('',#6544,#837);
#479=LINE('',#6546,#838);
#480=LINE('',#6548,#839);
#481=LINE('',#6550,#840);
#482=LINE('',#6552,#841);
#483=LINE('',#6554,#842);
#484=LINE('',#6556,#843);
#485=LINE('',#6558,#844);
#486=LINE('',#6560,#845);
#487=LINE('',#6562,#846);
#488=LINE('',#6564,#847);
#489=LINE('',#6566,#848);
#490=LINE('',#6568,#849);
#491=LINE('',#6570,#850);
#492=LINE('',#6572,#851);
#493=LINE('',#6574,#852);
#494=LINE('',#6576,#853);
#495=LINE('',#6577,#854);
#496=LINE('',#6580,#855);
#497=LINE('',#6583,#856);
#498=LINE('',#6586,#857);
#499=LINE('',#6589,#858);
#500=LINE('',#6592,#859);
#501=LINE('',#6595,#860);
#502=LINE('',#6598,#861);
#503=LINE('',#6601,#862);
#504=LINE('',#6603,#863);
#505=LINE('',#6605,#864);
#506=LINE('',#6609,#865);
#507=LINE('',#6611,#866);
#508=LINE('',#6623,#867);
#509=LINE('',#6624,#868);
#510=LINE('',#6626,#869);
#511=LINE('',#6627,#870);
#798=VECTOR('',#5132,1000.);
#799=VECTOR('',#5135,1000.);
#800=VECTOR('',#5140,1000.);
#801=VECTOR('',#5143,1000.);
#802=VECTOR('',#5148,1000.);
#803=VECTOR('',#5151,1000.);
#804=VECTOR('',#5156,6.);
#805=VECTOR('',#5163,10.);
#806=VECTOR('',#5170,10.);
#807=VECTOR('',#5181,5.);
#808=VECTOR('',#5186,5.);
#809=VECTOR('',#5193,5.);
#810=VECTOR('',#5202,5.);
#811=VECTOR('',#5209,5.);
#812=VECTOR('',#5216,5.);
#813=VECTOR('',#5223,1000.);
#814=VECTOR('',#5226,1000.);
#815=VECTOR('',#5229,1000.);
#816=VECTOR('',#5230,1000.);
#817=VECTOR('',#5231,1000.);
#818=VECTOR('',#5232,1000.);
#819=VECTOR('',#5233,1000.);
#820=VECTOR('',#5234,1000.);
#821=VECTOR('',#5235,1000.);
#822=VECTOR('',#5236,1000.);
#823=VECTOR('',#5237,1000.);
#824=VECTOR('',#5238,1000.);
#825=VECTOR('',#5239,1000.);
#826=VECTOR('',#5240,1000.);
#827=VECTOR('',#5241,1000.);
#828=VECTOR('',#5242,1000.);
#829=VECTOR('',#5243,1000.);
#830=VECTOR('',#5244,1000.);
#831=VECTOR('',#5245,1000.);
#832=VECTOR('',#5246,1000.);
#833=VECTOR('',#5247,1000.);
#834=VECTOR('',#5248,1000.);
#835=VECTOR('',#5251,1000.);
#836=VECTOR('',#5252,1000.);
#837=VECTOR('',#5253,1000.);
#838=VECTOR('',#5254,1000.);
#839=VECTOR('',#5255,1000.);
#840=VECTOR('',#5256,1000.);
#841=VECTOR('',#5257,1000.);
#842=VECTOR('',#5258,1000.);
#843=VECTOR('',#5259,1000.);
#844=VECTOR('',#5260,1000.);
#845=VECTOR('',#5261,1000.);
#846=VECTOR('',#5262,1000.);
#847=VECTOR('',#5263,1000.);
#848=VECTOR('',#5264,1000.);
#849=VECTOR('',#5265,1000.);
#850=VECTOR('',#5266,1000.);
#851=VECTOR('',#5267,1000.);
#852=VECTOR('',#5268,1000.);
#853=VECTOR('',#5269,1000.);
#854=VECTOR('',#5270,1000.);
#855=VECTOR('',#5275,1000.);
#856=VECTOR('',#5280,1000.);
#857=VECTOR('',#5285,1000.);
#858=VECTOR('',#5290,1000.);
#859=VECTOR('',#5295,1000.);
#860=VECTOR('',#5300,1000.);
#861=VECTOR('',#5305,1000.);
#862=VECTOR('',#5310,1000.);
#863=VECTOR('',#5313,1000.);
#864=VECTOR('',#5316,1000.);
#865=VECTOR('',#5323,1000.);
#866=VECTOR('',#5326,1000.);
#867=VECTOR('',#5349,1000.);
#868=VECTOR('',#5350,1000.);
#869=VECTOR('',#5353,1000.);
#870=VECTOR('',#5354,1000.);
#1024=CYLINDRICAL_SURFACE('',#4382,1.5);
#1025=CYLINDRICAL_SURFACE('',#4385,2.5);
#1026=CYLINDRICAL_SURFACE('',#4388,2.5);
#1027=CYLINDRICAL_SURFACE('',#4391,6.);
#1028=CYLINDRICAL_SURFACE('',#4394,10.);
#1029=CYLINDRICAL_SURFACE('',#4397,10.);
#1030=CYLINDRICAL_SURFACE('',#4402,5.);
#1031=CYLINDRICAL_SURFACE('',#4404,5.);
#1032=CYLINDRICAL_SURFACE('',#4407,5.);
#1033=CYLINDRICAL_SURFACE('',#4411,5.);
#1034=CYLINDRICAL_SURFACE('',#4414,5.);
#1035=CYLINDRICAL_SURFACE('',#4417,5.);
#1036=CYLINDRICAL_SURFACE('',#4420,2.5);
#1037=CYLINDRICAL_SURFACE('',#4449,10.);
#1038=CYLINDRICAL_SURFACE('',#4450,10.);
#1039=CYLINDRICAL_SURFACE('',#4451,10.);
#1040=CYLINDRICAL_SURFACE('',#4452,10.);
#1166=FACE_OUTER_BOUND('',#1420,.T.);
#1167=FACE_OUTER_BOUND('',#1421,.T.);
#1168=FACE_OUTER_BOUND('',#1422,.T.);
#1169=FACE_OUTER_BOUND('',#1423,.T.);
#1170=FACE_OUTER_BOUND('',#1424,.T.);
#1171=FACE_OUTER_BOUND('',#1425,.T.);
#1172=FACE_OUTER_BOUND('',#1426,.T.);
#1173=FACE_OUTER_BOUND('',#1427,.T.);
#1174=FACE_OUTER_BOUND('',#1428,.T.);
#1175=FACE_OUTER_BOUND('',#1429,.T.);
#1176=FACE_OUTER_BOUND('',#1430,.T.);
#1177=FACE_OUTER_BOUND('',#1431,.T.);
#1178=FACE_OUTER_BOUND('',#1432,.T.);
#1179=FACE_OUTER_BOUND('',#1433,.T.);
#1180=FACE_OUTER_BOUND('',#1434,.T.);
#1181=FACE_OUTER_BOUND('',#1435,.T.);
#1182=FACE_OUTER_BOUND('',#1437,.T.);
#1183=FACE_OUTER_BOUND('',#1439,.T.);
#1184=FACE_OUTER_BOUND('',#1441,.T.);
#1185=FACE_OUTER_BOUND('',#1443,.T.);
#1186=FACE_OUTER_BOUND('',#1445,.T.);
#1187=FACE_OUTER_BOUND('',#1447,.T.);
#1188=FACE_OUTER_BOUND('',#1449,.T.);
#1189=FACE_OUTER_BOUND('',#1451,.T.);
#1190=FACE_OUTER_BOUND('',#1453,.T.);
#1191=FACE_OUTER_BOUND('',#1455,.T.);
#1192=FACE_OUTER_BOUND('',#1456,.T.);
#1193=FACE_OUTER_BOUND('',#1458,.T.);
#1194=FACE_OUTER_BOUND('',#1459,.T.);
#1195=FACE_OUTER_BOUND('',#1460,.T.);
#1196=FACE_OUTER_BOUND('',#1461,.T.);
#1197=FACE_OUTER_BOUND('',#1463,.T.);
#1198=FACE_OUTER_BOUND('',#1464,.T.);
#1199=FACE_OUTER_BOUND('',#1465,.T.);
#1200=FACE_OUTER_BOUND('',#1466,.T.);
#1201=FACE_OUTER_BOUND('',#1467,.T.);
#1202=FACE_OUTER_BOUND('',#1468,.T.);
#1203=FACE_OUTER_BOUND('',#1469,.T.);
#1204=FACE_OUTER_BOUND('',#1470,.T.);
#1205=FACE_OUTER_BOUND('',#1471,.T.);
#1206=FACE_OUTER_BOUND('',#1473,.T.);
#1207=FACE_OUTER_BOUND('',#1475,.T.);
#1208=FACE_OUTER_BOUND('',#1476,.T.);
#1209=FACE_OUTER_BOUND('',#1477,.T.);
#1210=FACE_OUTER_BOUND('',#1478,.T.);
#1420=EDGE_LOOP('',(#3152,#3153,#3154,#3155));
#1421=EDGE_LOOP('',(#3156,#3157,#3158,#3159));
#1422=EDGE_LOOP('',(#3160,#3161,#3162,#3163));
#1423=EDGE_LOOP('',(#3164,#3165,#3166,#3167));
#1424=EDGE_LOOP('',(#3168,#3169,#3170,#3171));
#1425=EDGE_LOOP('',(#3172,#3173,#3174,#3175));
#1426=EDGE_LOOP('',(#3176));
#1427=EDGE_LOOP('',(#3177,#3178,#3179,#3180));
#1428=EDGE_LOOP('',(#3181,#3182,#3183,#3184));
#1429=EDGE_LOOP('',(#3185,#3186,#3187,#3188));
#1430=EDGE_LOOP('',(#3189));
#1431=EDGE_LOOP('',(#3190,#3191,#3192,#3193));
#1432=EDGE_LOOP('',(#3194,#3195,#3196,#3197));
#1433=EDGE_LOOP('',(#3198,#3199,#3200,#3201));
#1434=EDGE_LOOP('',(#3202,#3203,#3204,#3205));
#1435=EDGE_LOOP('',(#3206,#3207,#3208,#3209,#3210,#3211,#3212,#3213,#3214,
#3215,#3216,#3217,#3218,#3219,#3220,#3221,#3222,#3223,#3224,#3225));
#1436=EDGE_LOOP('',(#3226));
#1437=EDGE_LOOP('',(#3227,#3228,#3229,#3230,#3231,#3232,#3233,#3234,#3235,
#3236,#3237,#3238,#3239,#3240,#3241,#3242,#3243,#3244,#3245,#3246));
#1438=EDGE_LOOP('',(#3247));
#1439=EDGE_LOOP('',(#3248,#3249,#3250,#3251));
#1440=EDGE_LOOP('',(#3252));
#1441=EDGE_LOOP('',(#3253,#3254,#3255,#3256));
#1442=EDGE_LOOP('',(#3257));
#1443=EDGE_LOOP('',(#3258,#3259,#3260,#3261));
#1444=EDGE_LOOP('',(#3262));
#1445=EDGE_LOOP('',(#3263,#3264,#3265,#3266));
#1446=EDGE_LOOP('',(#3267));
#1447=EDGE_LOOP('',(#3268,#3269,#3270,#3271));
#1448=EDGE_LOOP('',(#3272));
#1449=EDGE_LOOP('',(#3273,#3274,#3275,#3276));
#1450=EDGE_LOOP('',(#3277));
#1451=EDGE_LOOP('',(#3278,#3279,#3280,#3281));
#1452=EDGE_LOOP('',(#3282));
#1453=EDGE_LOOP('',(#3283,#3284,#3285,#3286));
#1454=EDGE_LOOP('',(#3287));
#1455=EDGE_LOOP('',(#3288,#3289,#3290,#3291));
#1456=EDGE_LOOP('',(#3292,#3293,#3294,#3295));
#1457=EDGE_LOOP('',(#3296,#3297));
#1458=EDGE_LOOP('',(#3298,#3299,#3300,#3301));
#1459=EDGE_LOOP('',(#3302,#3303,#3304,#3305));
#1460=EDGE_LOOP('',(#3306,#3307,#3308,#3309));
#1461=EDGE_LOOP('',(#3310,#3311,#3312,#3313));
#1462=EDGE_LOOP('',(#3314,#3315));
#1463=EDGE_LOOP('',(#3316,#3317,#3318,#3319));
#1464=EDGE_LOOP('',(#3320,#3321,#3322,#3323));
#1465=EDGE_LOOP('',(#3324,#3325,#3326,#3327));
#1466=EDGE_LOOP('',(#3328,#3329,#3330,#3331));
#1467=EDGE_LOOP('',(#3332,#3333,#3334,#3335));
#1468=EDGE_LOOP('',(#3336,#3337,#3338,#3339));
#1469=EDGE_LOOP('',(#3340));
#1470=EDGE_LOOP('',(#3341));
#1471=EDGE_LOOP('',(#3342));
#1472=EDGE_LOOP('',(#3343));
#1473=EDGE_LOOP('',(#3344));
#1474=EDGE_LOOP('',(#3345));
#1475=EDGE_LOOP('',(#3346,#3347,#3348,#3349,#3350,#3351));
#1476=EDGE_LOOP('',(#3352,#3353,#3354,#3355,#3356,#3357));
#1477=EDGE_LOOP('',(#3358,#3359,#3360,#3361));
#1478=EDGE_LOOP('',(#3362,#3363,#3364,#3365));
#1666=CIRCLE('',#4383,1.5);
#1667=CIRCLE('',#4384,1.5);
#1668=CIRCLE('',#4386,2.5);
#1669=CIRCLE('',#4387,2.5);
#1670=CIRCLE('',#4389,2.5);
#1671=CIRCLE('',#4390,2.5);
#1672=CIRCLE('',#4392,6.);
#1673=CIRCLE('',#4393,6.);
#1674=CIRCLE('',#4395,10.);
#1675=CIRCLE('',#4396,10.);
#1676=CIRCLE('',#4398,10.);
#1677=CIRCLE('',#4399,10.);
#1678=CIRCLE('',#4401,5.);
#1679=CIRCLE('',#4403,5.);
#1680=CIRCLE('',#4405,5.);
#1681=CIRCLE('',#4406,5.);
#1682=CIRCLE('',#4408,5.);
#1683=CIRCLE('',#4409,5.);
#1684=CIRCLE('',#4412,5.);
#1685=CIRCLE('',#4413,5.);
#1686=CIRCLE('',#4415,5.);
#1687=CIRCLE('',#4416,5.);
#1688=CIRCLE('',#4418,5.);
#1689=CIRCLE('',#4419,5.);
#1690=CIRCLE('',#4421,2.5);
#1691=CIRCLE('',#4422,2.5);
#1692=CIRCLE('',#4426,10.);
#1693=CIRCLE('',#4428,10.);
#1694=CIRCLE('',#4430,10.);
#1695=CIRCLE('',#4432,10.);
#1696=CIRCLE('',#4434,10.);
#1697=CIRCLE('',#4436,10.);
#1698=CIRCLE('',#4438,10.);
#1699=CIRCLE('',#4440,10.);
#1950=VERTEX_POINT('',#6409);
#1951=VERTEX_POINT('',#6410);
#1952=VERTEX_POINT('',#6412);
#1953=VERTEX_POINT('',#6414);
#1954=VERTEX_POINT('',#6418);
#1955=VERTEX_POINT('',#6419);
#1956=VERTEX_POINT('',#6421);
#1957=VERTEX_POINT('',#6423);
#1958=VERTEX_POINT('',#6427);
#1959=VERTEX_POINT('',#6428);
#1960=VERTEX_POINT('',#6430);
#1961=VERTEX_POINT('',#6432);
#1962=VERTEX_POINT('',#6436);
#1963=VERTEX_POINT('',#6438);
#1964=VERTEX_POINT('',#6442);
#1965=VERTEX_POINT('',#6444);
#1966=VERTEX_POINT('',#6448);
#1967=VERTEX_POINT('',#6450);
#1968=VERTEX_POINT('',#6454);
#1969=VERTEX_POINT('',#6457);
#1970=VERTEX_POINT('',#6461);
#1971=VERTEX_POINT('',#6463);
#1972=VERTEX_POINT('',#6467);
#1973=VERTEX_POINT('',#6469);
#1974=VERTEX_POINT('',#6474);
#1975=VERTEX_POINT('',#6476);
#1976=VERTEX_POINT('',#6480);
#1977=VERTEX_POINT('',#6482);
#1978=VERTEX_POINT('',#6486);
#1979=VERTEX_POINT('',#6488);
#1980=VERTEX_POINT('',#6497);
#1981=VERTEX_POINT('',#6498);
#1982=VERTEX_POINT('',#6500);
#1983=VERTEX_POINT('',#6502);
#1984=VERTEX_POINT('',#6504);
#1985=VERTEX_POINT('',#6506);
#1986=VERTEX_POINT('',#6508);
#1987=VERTEX_POINT('',#6510);
#1988=VERTEX_POINT('',#6512);
#1989=VERTEX_POINT('',#6514);
#1990=VERTEX_POINT('',#6516);
#1991=VERTEX_POINT('',#6518);
#1992=VERTEX_POINT('',#6520);
#1993=VERTEX_POINT('',#6522);
#1994=VERTEX_POINT('',#6524);
#1995=VERTEX_POINT('',#6526);
#1996=VERTEX_POINT('',#6528);
#1997=VERTEX_POINT('',#6530);
#1998=VERTEX_POINT('',#6532);
#1999=VERTEX_POINT('',#6534);
#2000=VERTEX_POINT('',#6538);
#2001=VERTEX_POINT('',#6539);
#2002=VERTEX_POINT('',#6541);
#2003=VERTEX_POINT('',#6543);
#2004=VERTEX_POINT('',#6545);
#2005=VERTEX_POINT('',#6547);
#2006=VERTEX_POINT('',#6549);
#2007=VERTEX_POINT('',#6551);
#2008=VERTEX_POINT('',#6553);
#2009=VERTEX_POINT('',#6555);
#2010=VERTEX_POINT('',#6557);
#2011=VERTEX_POINT('',#6559);
#2012=VERTEX_POINT('',#6561);
#2013=VERTEX_POINT('',#6563);
#2014=VERTEX_POINT('',#6565);
#2015=VERTEX_POINT('',#6567);
#2016=VERTEX_POINT('',#6569);
#2017=VERTEX_POINT('',#6571);
#2018=VERTEX_POINT('',#6573);
#2019=VERTEX_POINT('',#6575);
#2383=EDGE_CURVE('',#1950,#1951,#1666,.T.);
#2384=EDGE_CURVE('',#1950,#1952,#439,.T.);
#2385=EDGE_CURVE('',#1952,#1953,#1667,.T.);
#2386=EDGE_CURVE('',#1951,#1953,#440,.T.);
#2387=EDGE_CURVE('',#1954,#1955,#1668,.T.);
#2388=EDGE_CURVE('',#1954,#1956,#441,.T.);
#2389=EDGE_CURVE('',#1956,#1957,#1669,.T.);
#2390=EDGE_CURVE('',#1955,#1957,#442,.T.);
#2391=EDGE_CURVE('',#1958,#1959,#1670,.T.);
#2392=EDGE_CURVE('',#1958,#1960,#443,.T.);
#2393=EDGE_CURVE('',#1960,#1961,#1671,.T.);
#2394=EDGE_CURVE('',#1959,#1961,#444,.T.);
#2395=EDGE_CURVE('',#1962,#1962,#1672,.T.);
#2396=EDGE_CURVE('',#1962,#1963,#445,.T.);
#2397=EDGE_CURVE('',#1963,#1963,#1673,.T.);
#2398=EDGE_CURVE('',#1964,#1964,#1674,.T.);
#2399=EDGE_CURVE('',#1964,#1965,#446,.T.);
#2400=EDGE_CURVE('',#1965,#1965,#1675,.T.);
#2401=EDGE_CURVE('',#1966,#1966,#1676,.T.);
#2402=EDGE_CURVE('',#1966,#1967,#447,.T.);
#2403=EDGE_CURVE('',#1967,#1967,#1677,.T.);
#2404=EDGE_CURVE('',#1968,#1968,#1678,.T.);
#2405=EDGE_CURVE('',#1969,#1969,#1679,.T.);
#2406=EDGE_CURVE('',#1969,#1968,#448,.T.);
#2407=EDGE_CURVE('',#1970,#1970,#1680,.T.);
#2408=EDGE_CURVE('',#1970,#1971,#449,.T.);
#2409=EDGE_CURVE('',#1971,#1971,#1681,.T.);
#2410=EDGE_CURVE('',#1972,#1972,#1682,.T.);
#2411=EDGE_CURVE('',#1972,#1973,#450,.T.);
#2412=EDGE_CURVE('',#1973,#1973,#1683,.T.);
#2413=EDGE_CURVE('',#1974,#1974,#1684,.T.);
#2414=EDGE_CURVE('',#1974,#1975,#451,.T.);
#2415=EDGE_CURVE('',#1975,#1975,#1685,.T.);
#2416=EDGE_CURVE('',#1976,#1976,#1686,.T.);
#2417=EDGE_CURVE('',#1976,#1977,#452,.T.);
#2418=EDGE_CURVE('',#1977,#1977,#1687,.T.);
#2419=EDGE_CURVE('',#1978,#1978,#1688,.T.);
#2420=EDGE_CURVE('',#1978,#1979,#453,.T.);
#2421=EDGE_CURVE('',#1979,#1979,#1689,.T.);
#2422=EDGE_CURVE('',#1959,#1958,#1690,.T.);
#2423=EDGE_CURVE('',#1957,#1959,#454,.T.);
#2424=EDGE_CURVE('',#1957,#1956,#1691,.T.);
#2425=EDGE_CURVE('',#1958,#1956,#455,.T.);
#2426=EDGE_CURVE('',#1980,#1981,#456,.T.);
#2427=EDGE_CURVE('',#1981,#1982,#457,.T.);
#2428=EDGE_CURVE('',#1982,#1983,#458,.T.);
#2429=EDGE_CURVE('',#1983,#1984,#459,.T.);
#2430=EDGE_CURVE('',#1984,#1985,#460,.T.);
#2431=EDGE_CURVE('',#1985,#1986,#461,.T.);
#2432=EDGE_CURVE('',#1986,#1987,#462,.T.);
#2433=EDGE_CURVE('',#1987,#1988,#463,.T.);
#2434=EDGE_CURVE('',#1988,#1989,#464,.T.);
#2435=EDGE_CURVE('',#1989,#1990,#465,.T.);
#2436=EDGE_CURVE('',#1990,#1991,#466,.T.);
#2437=EDGE_CURVE('',#1992,#1991,#467,.T.);
#2438=EDGE_CURVE('',#1992,#1993,#468,.T.);
#2439=EDGE_CURVE('',#1993,#1994,#469,.T.);
#2440=EDGE_CURVE('',#1994,#1995,#470,.T.);
#2441=EDGE_CURVE('',#1996,#1995,#471,.T.);
#2442=EDGE_CURVE('',#1996,#1997,#472,.T.);
#2443=EDGE_CURVE('',#1997,#1998,#473,.T.);
#2444=EDGE_CURVE('',#1998,#1999,#474,.T.);
#2445=EDGE_CURVE('',#1999,#1980,#475,.T.);
#2446=EDGE_CURVE('',#2000,#2001,#476,.T.);
#2447=EDGE_CURVE('',#2002,#2000,#477,.T.);
#2448=EDGE_CURVE('',#2003,#2002,#478,.T.);
#2449=EDGE_CURVE('',#2004,#2003,#479,.T.);
#2450=EDGE_CURVE('',#2005,#2004,#480,.T.);
#2451=EDGE_CURVE('',#2006,#2005,#481,.T.);
#2452=EDGE_CURVE('',#2006,#2007,#482,.T.);
#2453=EDGE_CURVE('',#2008,#2007,#483,.T.);
#2454=EDGE_CURVE('',#2009,#2008,#484,.T.);
#2455=EDGE_CURVE('',#2010,#2009,#485,.T.);
#2456=EDGE_CURVE('',#2010,#2011,#486,.T.);
#2457=EDGE_CURVE('',#2012,#2011,#487,.T.);
#2458=EDGE_CURVE('',#2013,#2012,#488,.T.);
#2459=EDGE_CURVE('',#2014,#2013,#489,.T.);
#2460=EDGE_CURVE('',#2015,#2014,#490,.T.);
#2461=EDGE_CURVE('',#2016,#2015,#491,.T.);
#2462=EDGE_CURVE('',#2017,#2016,#492,.T.);
#2463=EDGE_CURVE('',#2018,#2017,#493,.T.);
#2464=EDGE_CURVE('',#2019,#2018,#494,.T.);
#2465=EDGE_CURVE('',#2001,#2019,#495,.T.);
#2466=EDGE_CURVE('',#1991,#2011,#1692,.T.);
#2467=EDGE_CURVE('',#1990,#2012,#496,.T.);
#2468=EDGE_CURVE('',#2010,#1992,#1693,.T.);
#2469=EDGE_CURVE('',#1993,#2009,#497,.T.);
#2470=EDGE_CURVE('',#1995,#2007,#1694,.T.);
#2471=EDGE_CURVE('',#1994,#2008,#498,.T.);
#2472=EDGE_CURVE('',#2006,#1996,#1695,.T.);
#2473=EDGE_CURVE('',#1997,#2005,#499,.T.);
#2474=EDGE_CURVE('',#1981,#2000,#1696,.T.);
#2475=EDGE_CURVE('',#1980,#2002,#500,.T.);
#2476=EDGE_CURVE('',#2001,#1982,#1697,.T.);
#2477=EDGE_CURVE('',#1983,#2019,#501,.T.);
#2478=EDGE_CURVE('',#1985,#2017,#1698,.T.);
#2479=EDGE_CURVE('',#1984,#2018,#502,.T.);
#2480=EDGE_CURVE('',#2016,#1986,#1699,.T.);
#2481=EDGE_CURVE('',#1987,#2015,#503,.T.);
#2482=EDGE_CURVE('',#1988,#2014,#504,.T.);
#2483=EDGE_CURVE('',#1989,#2013,#505,.T.);
#2484=EDGE_CURVE('',#1998,#2004,#506,.T.);
#2485=EDGE_CURVE('',#1999,#2003,#507,.T.);
#2486=EDGE_CURVE('',#1953,#1960,#508,.T.);
#2487=EDGE_CURVE('',#1951,#1954,#509,.T.);
#2488=EDGE_CURVE('',#1961,#1952,#510,.T.);
#2489=EDGE_CURVE('',#1955,#1950,#511,.T.);
#3152=ORIENTED_EDGE('',*,*,#2383,.F.);
#3153=ORIENTED_EDGE('',*,*,#2384,.T.);
#3154=ORIENTED_EDGE('',*,*,#2385,.T.);
#3155=ORIENTED_EDGE('',*,*,#2386,.F.);
#3156=ORIENTED_EDGE('',*,*,#2387,.F.);
#3157=ORIENTED_EDGE('',*,*,#2388,.T.);
#3158=ORIENTED_EDGE('',*,*,#2389,.T.);
#3159=ORIENTED_EDGE('',*,*,#2390,.F.);
#3160=ORIENTED_EDGE('',*,*,#2391,.F.);
#3161=ORIENTED_EDGE('',*,*,#2392,.T.);
#3162=ORIENTED_EDGE('',*,*,#2393,.T.);
#3163=ORIENTED_EDGE('',*,*,#2394,.F.);
#3164=ORIENTED_EDGE('',*,*,#2395,.T.);
#3165=ORIENTED_EDGE('',*,*,#2396,.T.);
#3166=ORIENTED_EDGE('',*,*,#2397,.F.);
#3167=ORIENTED_EDGE('',*,*,#2396,.F.);
#3168=ORIENTED_EDGE('',*,*,#2398,.T.);
#3169=ORIENTED_EDGE('',*,*,#2399,.T.);
#3170=ORIENTED_EDGE('',*,*,#2400,.F.);
#3171=ORIENTED_EDGE('',*,*,#2399,.F.);
#3172=ORIENTED_EDGE('',*,*,#2401,.T.);
#3173=ORIENTED_EDGE('',*,*,#2402,.T.);
#3174=ORIENTED_EDGE('',*,*,#2403,.T.);
#3175=ORIENTED_EDGE('',*,*,#2402,.F.);
#3176=ORIENTED_EDGE('',*,*,#2404,.T.);
#3177=ORIENTED_EDGE('',*,*,#2405,.T.);
#3178=ORIENTED_EDGE('',*,*,#2406,.T.);
#3179=ORIENTED_EDGE('',*,*,#2404,.F.);
#3180=ORIENTED_EDGE('',*,*,#2406,.F.);
#3181=ORIENTED_EDGE('',*,*,#2407,.T.);
#3182=ORIENTED_EDGE('',*,*,#2408,.T.);
#3183=ORIENTED_EDGE('',*,*,#2409,.T.);
#3184=ORIENTED_EDGE('',*,*,#2408,.F.);
#3185=ORIENTED_EDGE('',*,*,#2410,.T.);
#3186=ORIENTED_EDGE('',*,*,#2411,.T.);
#3187=ORIENTED_EDGE('',*,*,#2412,.T.);
#3188=ORIENTED_EDGE('',*,*,#2411,.F.);
#3189=ORIENTED_EDGE('',*,*,#2410,.F.);
#3190=ORIENTED_EDGE('',*,*,#2413,.T.);
#3191=ORIENTED_EDGE('',*,*,#2414,.T.);
#3192=ORIENTED_EDGE('',*,*,#2415,.T.);
#3193=ORIENTED_EDGE('',*,*,#2414,.F.);
#3194=ORIENTED_EDGE('',*,*,#2416,.T.);
#3195=ORIENTED_EDGE('',*,*,#2417,.T.);
#3196=ORIENTED_EDGE('',*,*,#2418,.T.);
#3197=ORIENTED_EDGE('',*,*,#2417,.F.);
#3198=ORIENTED_EDGE('',*,*,#2419,.T.);
#3199=ORIENTED_EDGE('',*,*,#2420,.T.);
#3200=ORIENTED_EDGE('',*,*,#2421,.F.);
#3201=ORIENTED_EDGE('',*,*,#2420,.F.);
#3202=ORIENTED_EDGE('',*,*,#2422,.F.);
#3203=ORIENTED_EDGE('',*,*,#2423,.F.);
#3204=ORIENTED_EDGE('',*,*,#2424,.T.);
#3205=ORIENTED_EDGE('',*,*,#2425,.F.);
#3206=ORIENTED_EDGE('',*,*,#2426,.T.);
#3207=ORIENTED_EDGE('',*,*,#2427,.T.);
#3208=ORIENTED_EDGE('',*,*,#2428,.T.);
#3209=ORIENTED_EDGE('',*,*,#2429,.T.);
#3210=ORIENTED_EDGE('',*,*,#2430,.T.);
#3211=ORIENTED_EDGE('',*,*,#2431,.T.);
#3212=ORIENTED_EDGE('',*,*,#2432,.T.);
#3213=ORIENTED_EDGE('',*,*,#2433,.T.);
#3214=ORIENTED_EDGE('',*,*,#2434,.T.);
#3215=ORIENTED_EDGE('',*,*,#2435,.T.);
#3216=ORIENTED_EDGE('',*,*,#2436,.T.);
#3217=ORIENTED_EDGE('',*,*,#2437,.F.);
#3218=ORIENTED_EDGE('',*,*,#2438,.T.);
#3219=ORIENTED_EDGE('',*,*,#2439,.T.);
#3220=ORIENTED_EDGE('',*,*,#2440,.T.);
#3221=ORIENTED_EDGE('',*,*,#2441,.F.);
#3222=ORIENTED_EDGE('',*,*,#2442,.T.);
#3223=ORIENTED_EDGE('',*,*,#2443,.T.);
#3224=ORIENTED_EDGE('',*,*,#2444,.T.);
#3225=ORIENTED_EDGE('',*,*,#2445,.T.);
#3226=ORIENTED_EDGE('',*,*,#2398,.F.);
#3227=ORIENTED_EDGE('',*,*,#2446,.F.);
#3228=ORIENTED_EDGE('',*,*,#2447,.F.);
#3229=ORIENTED_EDGE('',*,*,#2448,.F.);
#3230=ORIENTED_EDGE('',*,*,#2449,.F.);
#3231=ORIENTED_EDGE('',*,*,#2450,.F.);
#3232=ORIENTED_EDGE('',*,*,#2451,.F.);
#3233=ORIENTED_EDGE('',*,*,#2452,.T.);
#3234=ORIENTED_EDGE('',*,*,#2453,.F.);
#3235=ORIENTED_EDGE('',*,*,#2454,.F.);
#3236=ORIENTED_EDGE('',*,*,#2455,.F.);
#3237=ORIENTED_EDGE('',*,*,#2456,.T.);
#3238=ORIENTED_EDGE('',*,*,#2457,.F.);
#3239=ORIENTED_EDGE('',*,*,#2458,.F.);
#3240=ORIENTED_EDGE('',*,*,#2459,.F.);
#3241=ORIENTED_EDGE('',*,*,#2460,.F.);
#3242=ORIENTED_EDGE('',*,*,#2461,.F.);
#3243=ORIENTED_EDGE('',*,*,#2462,.F.);
#3244=ORIENTED_EDGE('',*,*,#2463,.F.);
#3245=ORIENTED_EDGE('',*,*,#2464,.F.);
#3246=ORIENTED_EDGE('',*,*,#2465,.F.);
#3247=ORIENTED_EDGE('',*,*,#2403,.F.);
#3248=ORIENTED_EDGE('',*,*,#2466,.F.);
#3249=ORIENTED_EDGE('',*,*,#2436,.F.);
#3250=ORIENTED_EDGE('',*,*,#2467,.T.);
#3251=ORIENTED_EDGE('',*,*,#2457,.T.);
#3252=ORIENTED_EDGE('',*,*,#2415,.F.);
#3253=ORIENTED_EDGE('',*,*,#2438,.F.);
#3254=ORIENTED_EDGE('',*,*,#2468,.F.);
#3255=ORIENTED_EDGE('',*,*,#2455,.T.);
#3256=ORIENTED_EDGE('',*,*,#2469,.F.);
#3257=ORIENTED_EDGE('',*,*,#2416,.F.);
#3258=ORIENTED_EDGE('',*,*,#2470,.F.);
#3259=ORIENTED_EDGE('',*,*,#2440,.F.);
#3260=ORIENTED_EDGE('',*,*,#2471,.T.);
#3261=ORIENTED_EDGE('',*,*,#2453,.T.);
#3262=ORIENTED_EDGE('',*,*,#2418,.F.);
#3263=ORIENTED_EDGE('',*,*,#2442,.F.);
#3264=ORIENTED_EDGE('',*,*,#2472,.F.);
#3265=ORIENTED_EDGE('',*,*,#2451,.T.);
#3266=ORIENTED_EDGE('',*,*,#2473,.F.);
#3267=ORIENTED_EDGE('',*,*,#2419,.F.);
#3268=ORIENTED_EDGE('',*,*,#2474,.F.);
#3269=ORIENTED_EDGE('',*,*,#2426,.F.);
#3270=ORIENTED_EDGE('',*,*,#2475,.T.);
#3271=ORIENTED_EDGE('',*,*,#2447,.T.);
#3272=ORIENTED_EDGE('',*,*,#2405,.F.);
#3273=ORIENTED_EDGE('',*,*,#2428,.F.);
#3274=ORIENTED_EDGE('',*,*,#2476,.F.);
#3275=ORIENTED_EDGE('',*,*,#2465,.T.);
#3276=ORIENTED_EDGE('',*,*,#2477,.F.);
#3277=ORIENTED_EDGE('',*,*,#2409,.F.);
#3278=ORIENTED_EDGE('',*,*,#2478,.F.);
#3279=ORIENTED_EDGE('',*,*,#2430,.F.);
#3280=ORIENTED_EDGE('',*,*,#2479,.T.);
#3281=ORIENTED_EDGE('',*,*,#2463,.T.);
#3282=ORIENTED_EDGE('',*,*,#2407,.F.);
#3283=ORIENTED_EDGE('',*,*,#2432,.F.);
#3284=ORIENTED_EDGE('',*,*,#2480,.F.);
#3285=ORIENTED_EDGE('',*,*,#2461,.T.);
#3286=ORIENTED_EDGE('',*,*,#2481,.F.);
#3287=ORIENTED_EDGE('',*,*,#2412,.F.);
#3288=ORIENTED_EDGE('',*,*,#2460,.T.);
#3289=ORIENTED_EDGE('',*,*,#2482,.F.);
#3290=ORIENTED_EDGE('',*,*,#2433,.F.);
#3291=ORIENTED_EDGE('',*,*,#2481,.T.);
#3292=ORIENTED_EDGE('',*,*,#2459,.T.);
#3293=ORIENTED_EDGE('',*,*,#2483,.F.);
#3294=ORIENTED_EDGE('',*,*,#2434,.F.);
#3295=ORIENTED_EDGE('',*,*,#2482,.T.);
#3296=ORIENTED_EDGE('',*,*,#2391,.T.);
#3297=ORIENTED_EDGE('',*,*,#2422,.T.);
#3298=ORIENTED_EDGE('',*,*,#2458,.T.);
#3299=ORIENTED_EDGE('',*,*,#2467,.F.);
#3300=ORIENTED_EDGE('',*,*,#2435,.F.);
#3301=ORIENTED_EDGE('',*,*,#2483,.T.);
#3302=ORIENTED_EDGE('',*,*,#2454,.T.);
#3303=ORIENTED_EDGE('',*,*,#2471,.F.);
#3304=ORIENTED_EDGE('',*,*,#2439,.F.);
#3305=ORIENTED_EDGE('',*,*,#2469,.T.);
#3306=ORIENTED_EDGE('',*,*,#2450,.T.);
#3307=ORIENTED_EDGE('',*,*,#2484,.F.);
#3308=ORIENTED_EDGE('',*,*,#2443,.F.);
#3309=ORIENTED_EDGE('',*,*,#2473,.T.);
#3310=ORIENTED_EDGE('',*,*,#2449,.T.);
#3311=ORIENTED_EDGE('',*,*,#2485,.F.);
#3312=ORIENTED_EDGE('',*,*,#2444,.F.);
#3313=ORIENTED_EDGE('',*,*,#2484,.T.);
#3314=ORIENTED_EDGE('',*,*,#2389,.F.);
#3315=ORIENTED_EDGE('',*,*,#2424,.F.);
#3316=ORIENTED_EDGE('',*,*,#2448,.T.);
#3317=ORIENTED_EDGE('',*,*,#2475,.F.);
#3318=ORIENTED_EDGE('',*,*,#2445,.F.);
#3319=ORIENTED_EDGE('',*,*,#2485,.T.);
#3320=ORIENTED_EDGE('',*,*,#2464,.T.);
#3321=ORIENTED_EDGE('',*,*,#2479,.F.);
#3322=ORIENTED_EDGE('',*,*,#2429,.F.);
#3323=ORIENTED_EDGE('',*,*,#2477,.T.);
#3324=ORIENTED_EDGE('',*,*,#2478,.T.);
#3325=ORIENTED_EDGE('',*,*,#2462,.T.);
#3326=ORIENTED_EDGE('',*,*,#2480,.T.);
#3327=ORIENTED_EDGE('',*,*,#2431,.F.);
#3328=ORIENTED_EDGE('',*,*,#2474,.T.);
#3329=ORIENTED_EDGE('',*,*,#2446,.T.);
#3330=ORIENTED_EDGE('',*,*,#2476,.T.);
#3331=ORIENTED_EDGE('',*,*,#2427,.F.);
#3332=ORIENTED_EDGE('',*,*,#2470,.T.);
#3333=ORIENTED_EDGE('',*,*,#2452,.F.);
#3334=ORIENTED_EDGE('',*,*,#2472,.T.);
#3335=ORIENTED_EDGE('',*,*,#2441,.T.);
#3336=ORIENTED_EDGE('',*,*,#2466,.T.);
#3337=ORIENTED_EDGE('',*,*,#2456,.F.);
#3338=ORIENTED_EDGE('',*,*,#2468,.T.);
#3339=ORIENTED_EDGE('',*,*,#2437,.T.);
#3340=ORIENTED_EDGE('',*,*,#2421,.T.);
#3341=ORIENTED_EDGE('',*,*,#2413,.F.);
#3342=ORIENTED_EDGE('',*,*,#2400,.T.);
#3343=ORIENTED_EDGE('',*,*,#2395,.F.);
#3344=ORIENTED_EDGE('',*,*,#2401,.F.);
#3345=ORIENTED_EDGE('',*,*,#2397,.T.);
#3346=ORIENTED_EDGE('',*,*,#2486,.T.);
#3347=ORIENTED_EDGE('',*,*,#2392,.F.);
#3348=ORIENTED_EDGE('',*,*,#2425,.T.);
#3349=ORIENTED_EDGE('',*,*,#2388,.F.);
#3350=ORIENTED_EDGE('',*,*,#2487,.F.);
#3351=ORIENTED_EDGE('',*,*,#2386,.T.);
#3352=ORIENTED_EDGE('',*,*,#2488,.T.);
#3353=ORIENTED_EDGE('',*,*,#2384,.F.);
#3354=ORIENTED_EDGE('',*,*,#2489,.F.);
#3355=ORIENTED_EDGE('',*,*,#2390,.T.);
#3356=ORIENTED_EDGE('',*,*,#2423,.T.);
#3357=ORIENTED_EDGE('',*,*,#2394,.T.);
#3358=ORIENTED_EDGE('',*,*,#2383,.T.);
#3359=ORIENTED_EDGE('',*,*,#2487,.T.);
#3360=ORIENTED_EDGE('',*,*,#2387,.T.);
#3361=ORIENTED_EDGE('',*,*,#2489,.T.);
#3362=ORIENTED_EDGE('',*,*,#2385,.F.);
#3363=ORIENTED_EDGE('',*,*,#2488,.F.);
#3364=ORIENTED_EDGE('',*,*,#2393,.F.);
#3365=ORIENTED_EDGE('',*,*,#2486,.F.);
#4001=ADVANCED_FACE('',(#1166),#1024,.F.);
#4002=ADVANCED_FACE('',(#1167),#1025,.T.);
#4003=ADVANCED_FACE('',(#1168),#1026,.T.);
#4004=ADVANCED_FACE('',(#1169),#1027,.F.);
#4005=ADVANCED_FACE('',(#1170),#1028,.T.);
#4006=ADVANCED_FACE('',(#1171),#1029,.T.);
#4007=ADVANCED_FACE('',(#1172),#25,.T.);
#4008=ADVANCED_FACE('',(#1173),#1030,.T.);
#4009=ADVANCED_FACE('',(#1174),#1031,.T.);
#4010=ADVANCED_FACE('',(#1175),#1032,.T.);
#4011=ADVANCED_FACE('',(#1176),#26,.T.);
#4012=ADVANCED_FACE('',(#1177),#1033,.T.);
#4013=ADVANCED_FACE('',(#1178),#1034,.T.);
#4014=ADVANCED_FACE('',(#1179),#1035,.T.);
#4015=ADVANCED_FACE('',(#1180),#1036,.F.);
#4016=ADVANCED_FACE('',(#1181,#123),#218,.T.);
#4017=ADVANCED_FACE('',(#1182,#124),#219,.F.);
#4018=ADVANCED_FACE('',(#1183,#125),#220,.F.);
#4019=ADVANCED_FACE('',(#1184,#126),#221,.F.);
#4020=ADVANCED_FACE('',(#1185,#127),#222,.F.);
#4021=ADVANCED_FACE('',(#1186,#128),#223,.F.);
#4022=ADVANCED_FACE('',(#1187,#129),#224,.F.);
#4023=ADVANCED_FACE('',(#1188,#130),#225,.F.);
#4024=ADVANCED_FACE('',(#1189,#131),#226,.F.);
#4025=ADVANCED_FACE('',(#1190,#132),#227,.F.);
#4026=ADVANCED_FACE('',(#1191),#228,.F.);
#4027=ADVANCED_FACE('',(#1192,#133),#229,.F.);
#4028=ADVANCED_FACE('',(#1193),#230,.F.);
#4029=ADVANCED_FACE('',(#1194),#231,.F.);
#4030=ADVANCED_FACE('',(#1195),#232,.F.);
#4031=ADVANCED_FACE('',(#1196,#134),#233,.F.);
#4032=ADVANCED_FACE('',(#1197),#234,.F.);
#4033=ADVANCED_FACE('',(#1198),#235,.F.);
#4034=ADVANCED_FACE('',(#1199),#1037,.T.);
#4035=ADVANCED_FACE('',(#1200),#1038,.T.);
#4036=ADVANCED_FACE('',(#1201),#1039,.T.);
#4037=ADVANCED_FACE('',(#1202),#1040,.T.);
#4038=ADVANCED_FACE('',(#1203),#236,.T.);
#4039=ADVANCED_FACE('',(#1204),#237,.F.);
#4040=ADVANCED_FACE('',(#1205,#135),#238,.T.);
#4041=ADVANCED_FACE('',(#1206,#136),#239,.F.);
#4042=ADVANCED_FACE('',(#1207),#240,.F.);
#4043=ADVANCED_FACE('',(#1208),#241,.F.);
#4044=ADVANCED_FACE('',(#1209),#242,.T.);
#4045=ADVANCED_FACE('',(#1210),#243,.F.);
#4166=CLOSED_SHELL('',(#4001,#4002,#4003,#4004,#4005,#4006,#4007,#4008,
#4009,#4010,#4011,#4012,#4013,#4014,#4015,#4016,#4017,#4018,#4019,#4020,
#4021,#4022,#4023,#4024,#4025,#4026,#4027,#4028,#4029,#4030,#4031,#4032,
#4033,#4034,#4035,#4036,#4037,#4038,#4039,#4040,#4041,#4042,#4043,#4044,
#4045));
#4381=AXIS2_PLACEMENT_3D('',#6407,#5126,#5127);
#4382=AXIS2_PLACEMENT_3D('',#6408,#5128,#5129);
#4383=AXIS2_PLACEMENT_3D('',#6411,#5130,#5131);
#4384=AXIS2_PLACEMENT_3D('',#6415,#5133,#5134);
#4385=AXIS2_PLACEMENT_3D('',#6417,#5136,#5137);
#4386=AXIS2_PLACEMENT_3D('',#6420,#5138,#5139);
#4387=AXIS2_PLACEMENT_3D('',#6424,#5141,#5142);
#4388=AXIS2_PLACEMENT_3D('',#6426,#5144,#5145);
#4389=AXIS2_PLACEMENT_3D('',#6429,#5146,#5147);
#4390=AXIS2_PLACEMENT_3D('',#6433,#5149,#5150);
#4391=AXIS2_PLACEMENT_3D('',#6435,#5152,#5153);
#4392=AXIS2_PLACEMENT_3D('',#6437,#5154,#5155);
#4393=AXIS2_PLACEMENT_3D('',#6440,#5157,#5158);
#4394=AXIS2_PLACEMENT_3D('',#6441,#5159,#5160);
#4395=AXIS2_PLACEMENT_3D('',#6443,#5161,#5162);
#4396=AXIS2_PLACEMENT_3D('',#6446,#5164,#5165);
#4397=AXIS2_PLACEMENT_3D('',#6447,#5166,#5167);
#4398=AXIS2_PLACEMENT_3D('',#6449,#5168,#5169);
#4399=AXIS2_PLACEMENT_3D('',#6452,#5171,#5172);
#4400=AXIS2_PLACEMENT_3D('',#6453,#5173,#5174);
#4401=AXIS2_PLACEMENT_3D('',#6455,#5175,#5176);
#4402=AXIS2_PLACEMENT_3D('',#6456,#5177,#5178);
#4403=AXIS2_PLACEMENT_3D('',#6458,#5179,#5180);
#4404=AXIS2_PLACEMENT_3D('',#6460,#5182,#5183);
#4405=AXIS2_PLACEMENT_3D('',#6462,#5184,#5185);
#4406=AXIS2_PLACEMENT_3D('',#6465,#5187,#5188);
#4407=AXIS2_PLACEMENT_3D('',#6466,#5189,#5190);
#4408=AXIS2_PLACEMENT_3D('',#6468,#5191,#5192);
#4409=AXIS2_PLACEMENT_3D('',#6471,#5194,#5195);
#4410=AXIS2_PLACEMENT_3D('',#6472,#5196,#5197);
#4411=AXIS2_PLACEMENT_3D('',#6473,#5198,#5199);
#4412=AXIS2_PLACEMENT_3D('',#6475,#5200,#5201);
#4413=AXIS2_PLACEMENT_3D('',#6478,#5203,#5204);
#4414=AXIS2_PLACEMENT_3D('',#6479,#5205,#5206);
#4415=AXIS2_PLACEMENT_3D('',#6481,#5207,#5208);
#4416=AXIS2_PLACEMENT_3D('',#6484,#5210,#5211);
#4417=AXIS2_PLACEMENT_3D('',#6485,#5212,#5213);
#4418=AXIS2_PLACEMENT_3D('',#6487,#5214,#5215);
#4419=AXIS2_PLACEMENT_3D('',#6490,#5217,#5218);
#4420=AXIS2_PLACEMENT_3D('',#6491,#5219,#5220);
#4421=AXIS2_PLACEMENT_3D('',#6492,#5221,#5222);
#4422=AXIS2_PLACEMENT_3D('',#6494,#5224,#5225);
#4423=AXIS2_PLACEMENT_3D('',#6496,#5227,#5228);
#4424=AXIS2_PLACEMENT_3D('',#6537,#5249,#5250);
#4425=AXIS2_PLACEMENT_3D('',#6578,#5271,#5272);
#4426=AXIS2_PLACEMENT_3D('',#6579,#5273,#5274);
#4427=AXIS2_PLACEMENT_3D('',#6581,#5276,#5277);
#4428=AXIS2_PLACEMENT_3D('',#6582,#5278,#5279);
#4429=AXIS2_PLACEMENT_3D('',#6584,#5281,#5282);
#4430=AXIS2_PLACEMENT_3D('',#6585,#5283,#5284);
#4431=AXIS2_PLACEMENT_3D('',#6587,#5286,#5287);
#4432=AXIS2_PLACEMENT_3D('',#6588,#5288,#5289);
#4433=AXIS2_PLACEMENT_3D('',#6590,#5291,#5292);
#4434=AXIS2_PLACEMENT_3D('',#6591,#5293,#5294);
#4435=AXIS2_PLACEMENT_3D('',#6593,#5296,#5297);
#4436=AXIS2_PLACEMENT_3D('',#6594,#5298,#5299);
#4437=AXIS2_PLACEMENT_3D('',#6596,#5301,#5302);
#4438=AXIS2_PLACEMENT_3D('',#6597,#5303,#5304);
#4439=AXIS2_PLACEMENT_3D('',#6599,#5306,#5307);
#4440=AXIS2_PLACEMENT_3D('',#6600,#5308,#5309);
#4441=AXIS2_PLACEMENT_3D('',#6602,#5311,#5312);
#4442=AXIS2_PLACEMENT_3D('',#6604,#5314,#5315);
#4443=AXIS2_PLACEMENT_3D('',#6606,#5317,#5318);
#4444=AXIS2_PLACEMENT_3D('',#6607,#5319,#5320);
#4445=AXIS2_PLACEMENT_3D('',#6608,#5321,#5322);
#4446=AXIS2_PLACEMENT_3D('',#6610,#5324,#5325);
#4447=AXIS2_PLACEMENT_3D('',#6612,#5327,#5328);
#4448=AXIS2_PLACEMENT_3D('',#6613,#5329,#5330);
#4449=AXIS2_PLACEMENT_3D('',#6614,#5331,#5332);
#4450=AXIS2_PLACEMENT_3D('',#6615,#5333,#5334);
#4451=AXIS2_PLACEMENT_3D('',#6616,#5335,#5336);
#4452=AXIS2_PLACEMENT_3D('',#6617,#5337,#5338);
#4453=AXIS2_PLACEMENT_3D('',#6618,#5339,#5340);
#4454=AXIS2_PLACEMENT_3D('',#6619,#5341,#5342);
#4455=AXIS2_PLACEMENT_3D('',#6620,#5343,#5344);
#4456=AXIS2_PLACEMENT_3D('',#6621,#5345,#5346);
#4457=AXIS2_PLACEMENT_3D('',#6622,#5347,#5348);
#4458=AXIS2_PLACEMENT_3D('',#6625,#5351,#5352);
#4459=AXIS2_PLACEMENT_3D('',#6628,#5355,#5356);
#4460=AXIS2_PLACEMENT_3D('',#6629,#5357,#5358);
#5126=DIRECTION('axis',(0.,0.,1.));
#5127=DIRECTION('refdir',(1.,0.,0.));
#5128=DIRECTION('center_axis',(-1.,0.,0.));
#5129=DIRECTION('ref_axis',(0.,0.,1.));
#5130=DIRECTION('center_axis',(-1.,0.,0.));
#5131=DIRECTION('ref_axis',(0.,0.,-1.));
#5132=DIRECTION('',(-1.,0.,0.));
#5133=DIRECTION('center_axis',(-1.,0.,0.));
#5134=DIRECTION('ref_axis',(0.,0.,-1.));
#5135=DIRECTION('',(-1.,0.,0.));
#5136=DIRECTION('center_axis',(-1.,0.,0.));
#5137=DIRECTION('ref_axis',(0.,0.,1.));
#5138=DIRECTION('center_axis',(1.,0.,0.));
#5139=DIRECTION('ref_axis',(0.,0.,-1.));
#5140=DIRECTION('',(-1.,0.,0.));
#5141=DIRECTION('center_axis',(1.,0.,0.));
#5142=DIRECTION('ref_axis',(0.,0.,-1.));
#5143=DIRECTION('',(-1.,0.,0.));
#5144=DIRECTION('center_axis',(-1.,0.,0.));
#5145=DIRECTION('ref_axis',(0.,0.,1.));
#5146=DIRECTION('center_axis',(1.,0.,0.));
#5147=DIRECTION('ref_axis',(0.,0.,-1.));
#5148=DIRECTION('',(-1.,0.,0.));
#5149=DIRECTION('center_axis',(1.,0.,0.));
#5150=DIRECTION('ref_axis',(0.,0.,-1.));
#5151=DIRECTION('',(-1.,0.,0.));
#5152=DIRECTION('center_axis',(0.,0.,-1.));
#5153=DIRECTION('ref_axis',(-1.,0.,0.));
#5154=DIRECTION('center_axis',(0.,0.,1.));
#5155=DIRECTION('ref_axis',(1.,0.,0.));
#5156=DIRECTION('',(0.,0.,-1.));
#5157=DIRECTION('center_axis',(0.,0.,1.));
#5158=DIRECTION('ref_axis',(1.,0.,0.));
#5159=DIRECTION('center_axis',(0.,0.,-1.));
#5160=DIRECTION('ref_axis',(-1.,0.,0.));
#5161=DIRECTION('center_axis',(0.,0.,1.));
#5162=DIRECTION('ref_axis',(1.,0.,0.));
#5163=DIRECTION('',(0.,0.,1.));
#5164=DIRECTION('center_axis',(0.,0.,1.));
#5165=DIRECTION('ref_axis',(1.,0.,0.));
#5166=DIRECTION('center_axis',(0.,0.,-1.));
#5167=DIRECTION('ref_axis',(-1.,0.,0.));
#5168=DIRECTION('center_axis',(0.,0.,1.));
#5169=DIRECTION('ref_axis',(1.,0.,0.));
#5170=DIRECTION('',(0.,0.,1.));
#5171=DIRECTION('center_axis',(0.,0.,-1.));
#5172=DIRECTION('ref_axis',(1.,0.,0.));
#5173=DIRECTION('center_axis',(0.,1.,0.));
#5174=DIRECTION('ref_axis',(1.,0.,0.));
#5175=DIRECTION('center_axis',(1.,0.,0.));
#5176=DIRECTION('ref_axis',(0.,0.,-1.));
#5177=DIRECTION('center_axis',(-1.,0.,0.));
#5178=DIRECTION('ref_axis',(0.,0.,1.));
#5179=DIRECTION('center_axis',(1.,-8.26058798084195E-17,0.));
#5180=DIRECTION('ref_axis',(-8.26058798084195E-17,-1.,0.));
#5181=DIRECTION('',(1.,0.,0.));
#5182=DIRECTION('center_axis',(-1.,0.,0.));
#5183=DIRECTION('ref_axis',(0.,0.,1.));
#5184=DIRECTION('center_axis',(1.,8.26058798084195E-17,0.));
#5185=DIRECTION('ref_axis',(8.26058798084195E-17,-1.,0.));
#5186=DIRECTION('',(1.,0.,0.));
#5187=DIRECTION('center_axis',(-1.,8.26058798084195E-17,0.));
#5188=DIRECTION('ref_axis',(8.26058798084195E-17,1.,0.));
#5189=DIRECTION('center_axis',(-1.,0.,0.));
#5190=DIRECTION('ref_axis',(0.,0.,1.));
#5191=DIRECTION('center_axis',(1.,0.,0.));
#5192=DIRECTION('ref_axis',(0.,0.,-1.));
#5193=DIRECTION('',(1.,0.,0.));
#5194=DIRECTION('center_axis',(-1.,-8.26058798084195E-17,0.));
#5195=DIRECTION('ref_axis',(8.26058798084195E-17,-1.,0.));
#5196=DIRECTION('center_axis',(0.,1.,-7.49879891330929E-33));
#5197=DIRECTION('ref_axis',(-1.,0.,-1.22464679914735E-16));
#5198=DIRECTION('center_axis',(-1.,0.,0.));
#5199=DIRECTION('ref_axis',(0.,0.,1.));
#5200=DIRECTION('center_axis',(1.,0.,0.));
#5201=DIRECTION('ref_axis',(0.,0.,-1.));
#5202=DIRECTION('',(1.,0.,0.));
#5203=DIRECTION('center_axis',(-1.,-8.26058798084195E-17,0.));
#5204=DIRECTION('ref_axis',(8.26058798084195E-17,-1.,0.));
#5205=DIRECTION('center_axis',(-1.,0.,0.));
#5206=DIRECTION('ref_axis',(0.,0.,1.));
#5207=DIRECTION('center_axis',(1.,-8.26058798084195E-17,0.));
#5208=DIRECTION('ref_axis',(-8.26058798084195E-17,-1.,0.));
#5209=DIRECTION('',(1.,0.,0.));
#5210=DIRECTION('center_axis',(-1.,-8.26058798084195E-17,0.));
#5211=DIRECTION('ref_axis',(-8.26058798084195E-17,1.,0.));
#5212=DIRECTION('center_axis',(-1.,0.,0.));
#5213=DIRECTION('ref_axis',(0.,0.,1.));
#5214=DIRECTION('center_axis',(1.,8.26058798084195E-17,0.));
#5215=DIRECTION('ref_axis',(8.26058798084195E-17,-1.,0.));
#5216=DIRECTION('',(1.,0.,0.));
#5217=DIRECTION('center_axis',(1.,0.,0.));
#5218=DIRECTION('ref_axis',(0.,0.,-1.));
#5219=DIRECTION('center_axis',(1.,0.,0.));
#5220=DIRECTION('ref_axis',(0.,0.,-1.));
#5221=DIRECTION('center_axis',(1.,0.,0.));
#5222=DIRECTION('ref_axis',(0.,0.,-1.));
#5223=DIRECTION('',(-1.,0.,0.));
#5224=DIRECTION('center_axis',(1.,0.,0.));
#5225=DIRECTION('ref_axis',(0.,0.,-1.));
#5226=DIRECTION('',(1.,0.,0.));
#5227=DIRECTION('center_axis',(0.,0.,1.));
#5228=DIRECTION('ref_axis',(1.,0.,0.));
#5229=DIRECTION('',(8.26058798084195E-17,1.,0.));
#5230=DIRECTION('',(-1.,0.,0.));
#5231=DIRECTION('',(-8.26058798084195E-17,-1.,0.));
#5232=DIRECTION('',(-1.,0.,0.));
#5233=DIRECTION('',(-8.26058798084195E-17,1.,0.));
#5234=DIRECTION('',(-1.,0.,0.));
#5235=DIRECTION('',(8.26058798084195E-17,-1.,0.));
#5236=DIRECTION('',(-1.,-3.85494105772624E-15,0.));
#5237=DIRECTION('',(0.,-1.,0.));
#5238=DIRECTION('',(1.,-3.85494105772624E-15,0.));
#5239=DIRECTION('',(-8.26058798084195E-17,-1.,0.));
#5240=DIRECTION('',(-1.,0.,0.));
#5241=DIRECTION('',(8.26058798084195E-17,1.,0.));
#5242=DIRECTION('',(1.,0.,0.));
#5243=DIRECTION('',(8.26058798084195E-17,-1.,0.));
#5244=DIRECTION('',(-1.,0.,0.));
#5245=DIRECTION('',(-8.26058798084195E-17,1.,0.));
#5246=DIRECTION('',(1.,3.85494105772624E-15,0.));
#5247=DIRECTION('',(0.,1.,0.));
#5248=DIRECTION('',(-1.,3.85494105772624E-15,0.));
#5249=DIRECTION('center_axis',(0.,0.,1.));
#5250=DIRECTION('ref_axis',(1.,0.,0.));
#5251=DIRECTION('',(-1.,0.,0.));
#5252=DIRECTION('',(8.26058798084195E-17,1.,0.));
#5253=DIRECTION('',(-1.,3.85494105772624E-15,0.));
#5254=DIRECTION('',(0.,1.,0.));
#5255=DIRECTION('',(1.,3.85494105772624E-15,0.));
#5256=DIRECTION('',(-8.26058798084195E-17,1.,0.));
#5257=DIRECTION('',(-1.,0.,0.));
#5258=DIRECTION('',(8.26058798084195E-17,-1.,0.));
#5259=DIRECTION('',(1.,0.,0.));
#5260=DIRECTION('',(8.26058798084195E-17,1.,0.));
#5261=DIRECTION('',(-1.,0.,0.));
#5262=DIRECTION('',(-8.26058798084195E-17,-1.,0.));
#5263=DIRECTION('',(1.,-3.85494105772624E-15,0.));
#5264=DIRECTION('',(0.,-1.,0.));
#5265=DIRECTION('',(-1.,-3.85494105772624E-15,0.));
#5266=DIRECTION('',(8.26058798084195E-17,-1.,0.));
#5267=DIRECTION('',(-1.,0.,0.));
#5268=DIRECTION('',(-8.26058798084195E-17,1.,0.));
#5269=DIRECTION('',(-1.,0.,0.));
#5270=DIRECTION('',(-8.26058798084195E-17,-1.,0.));
#5271=DIRECTION('center_axis',(1.,-8.26058798084195E-17,0.));
#5272=DIRECTION('ref_axis',(8.26058798084195E-17,1.,0.));
#5273=DIRECTION('center_axis',(1.,-8.26058798084195E-17,0.));
#5274=DIRECTION('ref_axis',(8.26058798084195E-17,1.,0.));
#5275=DIRECTION('',(0.,0.,-1.));
#5276=DIRECTION('center_axis',(-1.,8.26058798084195E-17,0.));
#5277=DIRECTION('ref_axis',(-8.26058798084195E-17,-1.,0.));
#5278=DIRECTION('center_axis',(-1.,8.26058798084195E-17,0.));
#5279=DIRECTION('ref_axis',(-8.26058798084195E-17,-1.,0.));
#5280=DIRECTION('',(0.,0.,-1.));
#5281=DIRECTION('center_axis',(1.,8.26058798084195E-17,0.));
#5282=DIRECTION('ref_axis',(-8.26058798084195E-17,1.,0.));
#5283=DIRECTION('center_axis',(1.,8.26058798084195E-17,0.));
#5284=DIRECTION('ref_axis',(-8.26058798084195E-17,1.,0.));
#5285=DIRECTION('',(0.,0.,-1.));
#5286=DIRECTION('center_axis',(-1.,-8.26058798084195E-17,0.));
#5287=DIRECTION('ref_axis',(8.26058798084195E-17,-1.,0.));
#5288=DIRECTION('center_axis',(-1.,-8.26058798084195E-17,0.));
#5289=DIRECTION('ref_axis',(8.26058798084195E-17,-1.,0.));
#5290=DIRECTION('',(0.,0.,-1.));
#5291=DIRECTION('center_axis',(-1.,8.26058798084195E-17,0.));
#5292=DIRECTION('ref_axis',(-8.26058798084195E-17,-1.,0.));
#5293=DIRECTION('center_axis',(-1.,8.26058798084195E-17,0.));
#5294=DIRECTION('ref_axis',(-8.26058798084195E-17,-1.,0.));
#5295=DIRECTION('',(0.,0.,-1.));
#5296=DIRECTION('center_axis',(1.,-8.26058798084195E-17,0.));
#5297=DIRECTION('ref_axis',(8.26058798084195E-17,1.,0.));
#5298=DIRECTION('center_axis',(1.,-8.26058798084195E-17,0.));
#5299=DIRECTION('ref_axis',(8.26058798084195E-17,1.,0.));
#5300=DIRECTION('',(0.,0.,-1.));
#5301=DIRECTION('center_axis',(-1.,-8.26058798084195E-17,0.));
#5302=DIRECTION('ref_axis',(8.26058798084195E-17,-1.,0.));
#5303=DIRECTION('center_axis',(-1.,-8.26058798084195E-17,0.));
#5304=DIRECTION('ref_axis',(8.26058798084195E-17,-1.,0.));
#5305=DIRECTION('',(0.,0.,-1.));
#5306=DIRECTION('center_axis',(1.,8.26058798084195E-17,0.));
#5307=DIRECTION('ref_axis',(-8.26058798084195E-17,1.,0.));
#5308=DIRECTION('center_axis',(1.,8.26058798084195E-17,0.));
#5309=DIRECTION('ref_axis',(-8.26058798084195E-17,1.,0.));
#5310=DIRECTION('',(0.,0.,-1.));
#5311=DIRECTION('center_axis',(3.85494105772624E-15,-1.,0.));
#5312=DIRECTION('ref_axis',(1.,3.85494105772624E-15,0.));
#5313=DIRECTION('',(0.,0.,-1.));
#5314=DIRECTION('center_axis',(1.,0.,0.));
#5315=DIRECTION('ref_axis',(0.,0.,-1.));
#5316=DIRECTION('',(0.,0.,-1.));
#5317=DIRECTION('center_axis',(3.85494105772624E-15,1.,0.));
#5318=DIRECTION('ref_axis',(-1.,3.85494105772624E-15,0.));
#5319=DIRECTION('center_axis',(0.,1.,0.));
#5320=DIRECTION('ref_axis',(0.,0.,1.));
#5321=DIRECTION('center_axis',(-3.85494105772624E-15,1.,0.));
#5322=DIRECTION('ref_axis',(-1.,-3.85494105772624E-15,0.));
#5323=DIRECTION('',(0.,0.,-1.));
#5324=DIRECTION('center_axis',(-1.,0.,0.));
#5325=DIRECTION('ref_axis',(0.,0.,1.));
#5326=DIRECTION('',(0.,0.,-1.));
#5327=DIRECTION('center_axis',(-3.85494105772624E-15,-1.,0.));
#5328=DIRECTION('ref_axis',(1.,-3.85494105772624E-15,0.));
#5329=DIRECTION('center_axis',(0.,-1.,0.));
#5330=DIRECTION('ref_axis',(0.,0.,-1.));
#5331=DIRECTION('center_axis',(-1.,0.,0.));
#5332=DIRECTION('ref_axis',(0.,0.,1.));
#5333=DIRECTION('center_axis',(-1.,0.,0.));
#5334=DIRECTION('ref_axis',(0.,0.,1.));
#5335=DIRECTION('center_axis',(-1.,0.,0.));
#5336=DIRECTION('ref_axis',(0.,0.,1.));
#5337=DIRECTION('center_axis',(-1.,0.,0.));
#5338=DIRECTION('ref_axis',(0.,0.,1.));
#5339=DIRECTION('center_axis',(1.,0.,0.));
#5340=DIRECTION('ref_axis',(0.,0.,-1.));
#5341=DIRECTION('center_axis',(1.,0.,0.));
#5342=DIRECTION('ref_axis',(0.,0.,-1.));
#5343=DIRECTION('center_axis',(0.,0.,1.));
#5344=DIRECTION('ref_axis',(1.,0.,0.));
#5345=DIRECTION('center_axis',(0.,0.,1.));
#5346=DIRECTION('ref_axis',(1.,0.,0.));
#5347=DIRECTION('center_axis',(0.,1.,0.));
#5348=DIRECTION('ref_axis',(0.,0.,1.));
#5349=DIRECTION('',(0.,0.,-1.));
#5350=DIRECTION('',(0.,0.,-1.));
#5351=DIRECTION('center_axis',(0.,-1.,0.));
#5352=DIRECTION('ref_axis',(0.,0.,-1.));
#5353=DIRECTION('',(0.,0.,1.));
#5354=DIRECTION('',(0.,0.,1.));
#5355=DIRECTION('center_axis',(1.,0.,0.));
#5356=DIRECTION('ref_axis',(0.,0.,-1.));
#5357=DIRECTION('center_axis',(1.,0.,0.));
#5358=DIRECTION('ref_axis',(0.,0.,-1.));
#6407=CARTESIAN_POINT('',(0.,0.,0.));
#6408=CARTESIAN_POINT('Origin',(14.,10.,0.));
#6409=CARTESIAN_POINT('',(14.,9.5,-1.4142135623731));
#6410=CARTESIAN_POINT('',(14.,10.5,-1.4142135623731));
#6411=CARTESIAN_POINT('Origin',(14.,10.,0.));
#6412=CARTESIAN_POINT('',(-14.,9.5,-1.4142135623731));
#6413=CARTESIAN_POINT('',(14.,9.5,-1.4142135623731));
#6414=CARTESIAN_POINT('',(-14.,10.5,-1.4142135623731));
#6415=CARTESIAN_POINT('Origin',(-14.,10.,0.));
#6416=CARTESIAN_POINT('',(14.,10.5,-1.4142135623731));
#6417=CARTESIAN_POINT('Origin',(14.,10.,0.));
#6418=CARTESIAN_POINT('',(14.,10.5,-2.44948974278318));
#6419=CARTESIAN_POINT('',(14.,9.5,-2.44948974278318));
#6420=CARTESIAN_POINT('Origin',(14.,10.,0.));
#6421=CARTESIAN_POINT('',(13.5,10.5,-2.44948974278318));
#6422=CARTESIAN_POINT('',(14.,10.5,-2.44948974278318));
#6423=CARTESIAN_POINT('',(13.5,9.5,-2.44948974278318));
#6424=CARTESIAN_POINT('Origin',(13.5,10.,0.));
#6425=CARTESIAN_POINT('',(14.,9.5,-2.44948974278318));
#6426=CARTESIAN_POINT('Origin',(14.,10.,0.));
#6427=CARTESIAN_POINT('',(-13.5,10.5,-2.44948974278318));
#6428=CARTESIAN_POINT('',(-13.5,9.5,-2.44948974278318));
#6429=CARTESIAN_POINT('Origin',(-13.5,10.,0.));
#6430=CARTESIAN_POINT('',(-14.,10.5,-2.44948974278318));
#6431=CARTESIAN_POINT('',(14.,10.5,-2.44948974278318));
#6432=CARTESIAN_POINT('',(-14.,9.5,-2.44948974278318));
#6433=CARTESIAN_POINT('Origin',(-14.,10.,0.));
#6434=CARTESIAN_POINT('',(14.,9.5,-2.44948974278318));
#6435=CARTESIAN_POINT('Origin',(0.,0.,10.1));
#6436=CARTESIAN_POINT('',(6.,-7.34788079488412E-16,10.1));
#6437=CARTESIAN_POINT('Origin',(0.,0.,10.1));
#6438=CARTESIAN_POINT('',(6.,-7.34788079488412E-16,-10.1));
#6439=CARTESIAN_POINT('',(6.,-7.34788079488412E-16,10.1));
#6440=CARTESIAN_POINT('Origin',(0.,0.,-10.1));
#6441=CARTESIAN_POINT('Origin',(0.,0.,10.1));
#6442=CARTESIAN_POINT('',(10.,-1.22464679914735E-15,10.));
#6443=CARTESIAN_POINT('Origin',(0.,0.,10.));
#6444=CARTESIAN_POINT('',(10.,-1.22464679914735E-15,10.1));
#6445=CARTESIAN_POINT('',(10.,-1.22464679914735E-15,10.1));
#6446=CARTESIAN_POINT('Origin',(0.,0.,10.1));
#6447=CARTESIAN_POINT('Origin',(0.,0.,10.1));
#6448=CARTESIAN_POINT('',(10.,-1.22464679914735E-15,-10.1));
#6449=CARTESIAN_POINT('Origin',(0.,0.,-10.1));
#6450=CARTESIAN_POINT('',(10.,-1.22464679914735E-15,-10.));
#6451=CARTESIAN_POINT('',(10.,-1.22464679914735E-15,10.1));
#6452=CARTESIAN_POINT('Origin',(0.,0.,-10.));
#6453=CARTESIAN_POINT('Origin',(7.75,28.,0.));
#6454=CARTESIAN_POINT('',(13.,28.,-5.));
#6455=CARTESIAN_POINT('Origin',(13.,28.,0.));
#6456=CARTESIAN_POINT('Origin',(13.,28.,0.));
#6457=CARTESIAN_POINT('',(9.,28.,-5.));
#6458=CARTESIAN_POINT('Origin',(9.,28.,0.));
#6459=CARTESIAN_POINT('',(13.,28.,-5.));
#6460=CARTESIAN_POINT('Origin',(13.,28.,0.));
#6461=CARTESIAN_POINT('',(-5.,28.,-5.));
#6462=CARTESIAN_POINT('Origin',(-5.,28.,0.));
#6463=CARTESIAN_POINT('',(5.,28.,-5.));
#6464=CARTESIAN_POINT('',(13.,28.,-5.));
#6465=CARTESIAN_POINT('Origin',(5.,28.,0.));
#6466=CARTESIAN_POINT('Origin',(13.,28.,0.));
#6467=CARTESIAN_POINT('',(-13.,28.,-5.));
#6468=CARTESIAN_POINT('Origin',(-13.,28.,0.));
#6469=CARTESIAN_POINT('',(-9.,28.,-5.));
#6470=CARTESIAN_POINT('',(13.,28.,-5.));
#6471=CARTESIAN_POINT('Origin',(-9.,28.,0.));
#6472=CARTESIAN_POINT('Origin',(-7.75,28.,0.));
#6473=CARTESIAN_POINT('Origin',(13.,-28.,0.));
#6474=CARTESIAN_POINT('',(-13.,-28.,-5.));
#6475=CARTESIAN_POINT('Origin',(-13.,-28.,0.));
#6476=CARTESIAN_POINT('',(-9.,-28.,-5.));
#6477=CARTESIAN_POINT('',(13.,-28.,-5.));
#6478=CARTESIAN_POINT('Origin',(-9.,-28.,0.));
#6479=CARTESIAN_POINT('Origin',(13.,-28.,0.));
#6480=CARTESIAN_POINT('',(-5.,-28.,-5.));
#6481=CARTESIAN_POINT('Origin',(-5.,-28.,0.));
#6482=CARTESIAN_POINT('',(5.,-28.,-5.));
#6483=CARTESIAN_POINT('',(13.,-28.,-5.));
#6484=CARTESIAN_POINT('Origin',(5.,-28.,0.));
#6485=CARTESIAN_POINT('Origin',(13.,-28.,0.));
#6486=CARTESIAN_POINT('',(9.,-28.,-5.));
#6487=CARTESIAN_POINT('Origin',(9.,-28.,0.));
#6488=CARTESIAN_POINT('',(13.,-28.,-5.));
#6489=CARTESIAN_POINT('',(13.,-28.,-5.));
#6490=CARTESIAN_POINT('Origin',(13.,-28.,0.));
#6491=CARTESIAN_POINT('Origin',(-15.,10.,0.));
#6492=CARTESIAN_POINT('Origin',(-13.5,10.,0.));
#6493=CARTESIAN_POINT('',(-15.,9.5,-2.44948974278318));
#6494=CARTESIAN_POINT('Origin',(13.5,10.,0.));
#6495=CARTESIAN_POINT('',(-15.,10.5,-2.44948974278318));
#6496=CARTESIAN_POINT('Origin',(-9.,17.,10.));
#6497=CARTESIAN_POINT('',(9.,17.,10.));
#6498=CARTESIAN_POINT('',(9.,28.,10.));
#6499=CARTESIAN_POINT('',(9.,17.,10.));
#6500=CARTESIAN_POINT('',(5.,28.,10.));
#6501=CARTESIAN_POINT('',(13.5,28.,10.));
#6502=CARTESIAN_POINT('',(5.,17.,10.));
#6503=CARTESIAN_POINT('',(5.,38.,10.));
#6504=CARTESIAN_POINT('',(-5.,17.,10.));
#6505=CARTESIAN_POINT('',(-5.,17.,10.));
#6506=CARTESIAN_POINT('',(-5.,28.,10.));
#6507=CARTESIAN_POINT('',(-5.,38.,10.));
#6508=CARTESIAN_POINT('',(-9.,28.,10.));
#6509=CARTESIAN_POINT('',(13.5,28.,10.));
#6510=CARTESIAN_POINT('',(-9.,17.,10.));
#6511=CARTESIAN_POINT('',(-9.,17.,10.));
#6512=CARTESIAN_POINT('',(-13.5,17.,10.));
#6513=CARTESIAN_POINT('',(-13.5,17.,10.));
#6514=CARTESIAN_POINT('',(-13.5,-17.,10.));
#6515=CARTESIAN_POINT('',(-13.5,-17.,10.));
#6516=CARTESIAN_POINT('',(-9.,-17.,10.));
#6517=CARTESIAN_POINT('',(-13.5,-17.,10.));
#6518=CARTESIAN_POINT('',(-9.,-28.,10.));
#6519=CARTESIAN_POINT('',(-9.,-17.,10.));
#6520=CARTESIAN_POINT('',(-5.,-28.,10.));
#6521=CARTESIAN_POINT('',(13.5,-28.,10.));
#6522=CARTESIAN_POINT('',(-5.,-17.,10.));
#6523=CARTESIAN_POINT('',(-5.,-38.,10.));
#6524=CARTESIAN_POINT('',(5.,-17.,10.));
#6525=CARTESIAN_POINT('',(-5.,-17.,10.));
#6526=CARTESIAN_POINT('',(5.,-28.,10.));
#6527=CARTESIAN_POINT('',(5.,-38.,10.));
#6528=CARTESIAN_POINT('',(9.,-28.,10.));
#6529=CARTESIAN_POINT('',(13.5,-28.,10.));
#6530=CARTESIAN_POINT('',(9.,-17.,10.));
#6531=CARTESIAN_POINT('',(9.,-17.,10.));
#6532=CARTESIAN_POINT('',(13.5,-17.,10.));
#6533=CARTESIAN_POINT('',(13.5,-17.,10.));
#6534=CARTESIAN_POINT('',(13.5,17.,10.));
#6535=CARTESIAN_POINT('',(13.5,-17.,10.));
#6536=CARTESIAN_POINT('',(13.5,17.,10.));
#6537=CARTESIAN_POINT('Origin',(-9.,17.,-10.));
#6538=CARTESIAN_POINT('',(9.,28.,-10.));
#6539=CARTESIAN_POINT('',(5.,28.,-10.));
#6540=CARTESIAN_POINT('',(13.5,28.,-10.));
#6541=CARTESIAN_POINT('',(9.,17.,-10.));
#6542=CARTESIAN_POINT('',(9.,17.,-10.));
#6543=CARTESIAN_POINT('',(13.5,17.,-10.));
#6544=CARTESIAN_POINT('',(13.5,17.,-10.));
#6545=CARTESIAN_POINT('',(13.5,-17.,-10.));
#6546=CARTESIAN_POINT('',(13.5,-17.,-10.));
#6547=CARTESIAN_POINT('',(9.,-17.,-10.));
#6548=CARTESIAN_POINT('',(13.5,-17.,-10.));
#6549=CARTESIAN_POINT('',(9.,-28.,-10.));
#6550=CARTESIAN_POINT('',(9.,-17.,-10.));
#6551=CARTESIAN_POINT('',(5.,-28.,-10.));
#6552=CARTESIAN_POINT('',(13.5,-28.,-10.));
#6553=CARTESIAN_POINT('',(5.,-17.,-10.));
#6554=CARTESIAN_POINT('',(5.,-38.,-10.));
#6555=CARTESIAN_POINT('',(-5.,-17.,-10.));
#6556=CARTESIAN_POINT('',(-5.,-17.,-10.));
#6557=CARTESIAN_POINT('',(-5.,-28.,-10.));
#6558=CARTESIAN_POINT('',(-5.,-38.,-10.));
#6559=CARTESIAN_POINT('',(-9.,-28.,-10.));
#6560=CARTESIAN_POINT('',(13.5,-28.,-10.));
#6561=CARTESIAN_POINT('',(-9.,-17.,-10.));
#6562=CARTESIAN_POINT('',(-9.,-17.,-10.));
#6563=CARTESIAN_POINT('',(-13.5,-17.,-10.));
#6564=CARTESIAN_POINT('',(-13.5,-17.,-10.));
#6565=CARTESIAN_POINT('',(-13.5,17.,-10.));
#6566=CARTESIAN_POINT('',(-13.5,-17.,-10.));
#6567=CARTESIAN_POINT('',(-9.,17.,-10.));
#6568=CARTESIAN_POINT('',(-13.5,17.,-10.));
#6569=CARTESIAN_POINT('',(-9.,28.,-10.));
#6570=CARTESIAN_POINT('',(-9.,17.,-10.));
#6571=CARTESIAN_POINT('',(-5.,28.,-10.));
#6572=CARTESIAN_POINT('',(13.5,28.,-10.));
#6573=CARTESIAN_POINT('',(-5.,17.,-10.));
#6574=CARTESIAN_POINT('',(-5.,38.,-10.));
#6575=CARTESIAN_POINT('',(5.,17.,-10.));
#6576=CARTESIAN_POINT('',(-5.,17.,-10.));
#6577=CARTESIAN_POINT('',(5.,38.,-10.));
#6578=CARTESIAN_POINT('Origin',(-9.,-17.,10.));
#6579=CARTESIAN_POINT('Origin',(-9.,-28.,0.));
#6580=CARTESIAN_POINT('',(-9.,-17.,10.));
#6581=CARTESIAN_POINT('Origin',(-5.,-38.,10.));
#6582=CARTESIAN_POINT('Origin',(-5.,-28.,0.));
#6583=CARTESIAN_POINT('',(-5.,-17.,10.));
#6584=CARTESIAN_POINT('Origin',(5.,-38.,10.));
#6585=CARTESIAN_POINT('Origin',(5.,-28.,0.));
#6586=CARTESIAN_POINT('',(5.,-17.,10.));
#6587=CARTESIAN_POINT('Origin',(9.,-17.,10.));
#6588=CARTESIAN_POINT('Origin',(9.,-28.,0.));
#6589=CARTESIAN_POINT('',(9.,-17.,10.));
#6590=CARTESIAN_POINT('Origin',(9.,17.,10.));
#6591=CARTESIAN_POINT('Origin',(9.,28.,0.));
#6592=CARTESIAN_POINT('',(9.,17.,10.));
#6593=CARTESIAN_POINT('Origin',(5.,38.,10.));
#6594=CARTESIAN_POINT('Origin',(5.,28.,0.));
#6595=CARTESIAN_POINT('',(5.,17.,10.));
#6596=CARTESIAN_POINT('Origin',(-5.,38.,10.));
#6597=CARTESIAN_POINT('Origin',(-5.,28.,0.));
#6598=CARTESIAN_POINT('',(-5.,17.,10.));
#6599=CARTESIAN_POINT('Origin',(-9.,17.,10.));
#6600=CARTESIAN_POINT('Origin',(-9.,28.,0.));
#6601=CARTESIAN_POINT('',(-9.,17.,10.));
#6602=CARTESIAN_POINT('Origin',(-13.5,17.,10.));
#6603=CARTESIAN_POINT('',(-13.5,17.,10.));
#6604=CARTESIAN_POINT('Origin',(-13.5,-17.,10.));
#6605=CARTESIAN_POINT('',(-13.5,-17.,10.));
#6606=CARTESIAN_POINT('Origin',(-13.5,-17.,10.));
#6607=CARTESIAN_POINT('Origin',(-5.,-17.,10.));
#6608=CARTESIAN_POINT('Origin',(13.5,-17.,10.));
#6609=CARTESIAN_POINT('',(13.5,-17.,10.));
#6610=CARTESIAN_POINT('Origin',(13.5,-17.,10.));
#6611=CARTESIAN_POINT('',(13.5,17.,10.));
#6612=CARTESIAN_POINT('Origin',(13.5,17.,10.));
#6613=CARTESIAN_POINT('Origin',(-5.,17.,10.));
#6614=CARTESIAN_POINT('Origin',(13.5,28.,0.));
#6615=CARTESIAN_POINT('Origin',(13.5,28.,0.));
#6616=CARTESIAN_POINT('Origin',(13.5,-28.,0.));
#6617=CARTESIAN_POINT('Origin',(13.5,-28.,0.));
#6618=CARTESIAN_POINT('Origin',(13.,-28.,0.));
#6619=CARTESIAN_POINT('Origin',(-13.,-28.,0.));
#6620=CARTESIAN_POINT('Origin',(0.,0.,10.1));
#6621=CARTESIAN_POINT('Origin',(0.,0.,-10.1));
#6622=CARTESIAN_POINT('Origin',(14.,10.5,-1.4142135623731));
#6623=CARTESIAN_POINT('',(-14.,10.5,-1.4142135623731));
#6624=CARTESIAN_POINT('',(14.,10.5,-1.4142135623731));
#6625=CARTESIAN_POINT('Origin',(14.,9.5,-1.4142135623731));
#6626=CARTESIAN_POINT('',(-14.,9.5,-1.4142135623731));
#6627=CARTESIAN_POINT('',(14.,9.5,-1.4142135623731));
#6628=CARTESIAN_POINT('Origin',(14.,10.,0.));
#6629=CARTESIAN_POINT('Origin',(-14.,10.,0.));
#7768=UNCERTAINTY_MEASURE_WITH_UNIT(LENGTH_MEASURE(0.01),#7784,
'DISTANCE_ACCURACY_VALUE',
'Maximum model space distance between geometric entities at asserted c
onnectivities');
#7773=UNCERTAINTY_MEASURE_WITH_UNIT(LENGTH_MEASURE(0.01),#7784,
'DISTANCE_ACCURACY_VALUE',
'Maximum model space distance between geometric entities at asserted c
onnectivities');
#7778=(
GEOMETRIC_REPRESENTATION_CONTEXT(3)
GLOBAL_UNCERTAINTY_ASSIGNED_CONTEXT((#7768))
GLOBAL_UNIT_ASSIGNED_CONTEXT((#7784,#7786,#7787))
REPRESENTATION_CONTEXT('','3D')
);
#7783=(
GEOMETRIC_REPRESENTATION_CONTEXT(3)
GLOBAL_UNCERTAINTY_ASSIGNED_CONTEXT((#7773))
GLOBAL_UNIT_ASSIGNED_CONTEXT((#7784,#7786,#7787))
REPRESENTATION_CONTEXT('','3D')
);
#7784=(
LENGTH_UNIT()
NAMED_UNIT(*)
SI_UNIT(.MILLI.,.METRE.)
);
#7786=(
NAMED_UNIT(*)
PLANE_ANGLE_UNIT()
SI_UNIT($,.RADIAN.)
);
#7787=(
NAMED_UNIT(*)
SI_UNIT($,.STERADIAN.)
SOLID_ANGLE_UNIT()
);
#7792=SHAPE_DEFINITION_REPRESENTATION(#7802,#7822);
#7802=PRODUCT_DEFINITION_SHAPE('',$,#7832);
#7822=SHAPE_REPRESENTATION('',(#4381),#7778);
#7827=PRODUCT_DEFINITION_CONTEXT('part definition',#7856,'design');
#7832=PRODUCT_DEFINITION('Nut','Nut',#7841,#7827);
#7841=PRODUCT_DEFINITION_FORMATION('',$,#7862);
#7856=APPLICATION_CONTEXT(
'Core Data for Automotive Mechanical Design Process');
#7857=PRODUCT_CONTEXT('part definition',#7856,'mechanical');
#7862=PRODUCT('Nut','Nut',$,(#7857));
#7869=PRESENTATION_STYLE_ASSIGNMENT((#7874));
#7874=SURFACE_STYLE_USAGE(.BOTH.,#7879);
#7879=SURFACE_SIDE_STYLE('',(#7884));
#7884=SURFACE_STYLE_FILL_AREA(#7889);
#7889=FILL_AREA_STYLE('Opaque(31,36,43)',(#7894));
#7894=FILL_AREA_STYLE_COLOUR('Opaque(31,36,43)',#7899);
#7899=COLOUR_RGB('Opaque(31,36,43)',0.12156862745098,0.141176470588235,
0.168627450980392);
ENDSEC;
END-ISO-10303-21;
